ISO-10303-21;
HEADER;
/* Generated by software containing ST-Developer
 * from STEP Tools, Inc. (www.steptools.com) 
 */

FILE_DESCRIPTION(
/* description */ ('Torque wrench calibration arm'),
/* implementation_level */ '2;1');

FILE_NAME(
/* name */ 'M4x10 Cap Screw.step',
/* time_stamp */ '2026-10-28T03:24:52-07:00',
/* author */ (''),
/* organization */ (''),
/* preprocessor_version */ 'ST-DEVELOPER v20.2',
/* originating_system */ 'Autodesk Translation Framework v15.17.0.0',
/* authorisation */ '');

FILE_SCHEMA (('AUTOMOTIVE_DESIGN { 1 0 10303 214 3 1 1 }'));
ENDSEC;

DATA;
#10=MECHANICAL_DESIGN_GEOMETRIC_PRESENTATION_REPRESENTATION('',(#479),#12783);
#13=ORIENTED_CLOSED_SHELL('',*,#6550,.F.);
#16=BREP_WITH_VOIDS('Body1',#6551,(#13));
#345=CONICAL_SURFACE('',#7786,0.325,0.785398163397448);
#346=CONICAL_SURFACE('',#7790,0.335,0.785398163397448);
#347=CONICAL_SURFACE('',#7794,0.21,0.463647609000806);
#388=SHAPE_REPRESENTATION_RELATIONSHIP('SRR','None',#12973,#425);
#425=ADVANCED_BREP_SHAPE_REPRESENTATION('',(#16),#12782);
#479=STYLED_ITEM('',(#13219),#16);
#651=FACE_BOUND('',#1783,.T.);
#864=PLANE('',#7774);
#865=PLANE('',#7775);
#866=PLANE('',#7776);
#867=PLANE('',#7777);
#868=PLANE('',#7778);
#869=PLANE('',#7779);
#870=PLANE('',#7780);
#871=PLANE('',#7781);
#872=PLANE('',#7782);
#873=PLANE('',#7784);
#874=PLANE('',#7792);
#1254=FACE_OUTER_BOUND('',#1769,.T.);
#1255=FACE_OUTER_BOUND('',#1770,.T.);
#1256=FACE_OUTER_BOUND('',#1771,.T.);
#1257=FACE_OUTER_BOUND('',#1772,.T.);
#1258=FACE_OUTER_BOUND('',#1773,.T.);
#1259=FACE_OUTER_BOUND('',#1774,.T.);
#1260=FACE_OUTER_BOUND('',#1775,.T.);
#1261=FACE_OUTER_BOUND('',#1776,.T.);
#1262=FACE_OUTER_BOUND('',#1777,.T.);
#1263=FACE_OUTER_BOUND('',#1778,.T.);
#1264=FACE_OUTER_BOUND('',#1779,.T.);
#1265=FACE_OUTER_BOUND('',#1780,.T.);
#1266=FACE_OUTER_BOUND('',#1781,.T.);
#1267=FACE_OUTER_BOUND('',#1782,.T.);
#1268=FACE_OUTER_BOUND('',#1784,.T.);
#1269=FACE_OUTER_BOUND('',#1785,.T.);
#1769=EDGE_LOOP('',(#5927,#5928,#5929,#5930));
#1770=EDGE_LOOP('',(#5931,#5932,#5933,#5934));
#1771=EDGE_LOOP('',(#5935,#5936,#5937,#5938));
#1772=EDGE_LOOP('',(#5939,#5940,#5941,#5942));
#1773=EDGE_LOOP('',(#5943,#5944,#5945,#5946));
#1774=EDGE_LOOP('',(#5947,#5948,#5949,#5950));
#1775=EDGE_LOOP('',(#5951,#5952,#5953,#5954,#5955,#5956));
#1776=EDGE_LOOP('',(#5957,#5958,#5959,#5960,#5961,#5962));
#1777=EDGE_LOOP('',(#5963));
#1778=EDGE_LOOP('',(#5964));
#1779=EDGE_LOOP('',(#5965,#5966,#5967,#5968));
#1780=EDGE_LOOP('',(#5969,#5970,#5971,#5972));
#1781=EDGE_LOOP('',(#5973,#5974,#5975,#5976));
#1782=EDGE_LOOP('',(#5977));
#1783=EDGE_LOOP('',(#5978));
#1784=EDGE_LOOP('',(#5979,#5980,#5981,#5982));
#1785=EDGE_LOOP('',(#5983,#5984,#5985,#5986));
#2178=LINE('',#12621,#2593);
#2179=LINE('',#12623,#2594);
#2180=LINE('',#12625,#2595);
#2181=LINE('',#12626,#2596);
#2182=LINE('',#12629,#2597);
#2183=LINE('',#12631,#2598);
#2184=LINE('',#12632,#2599);
#2185=LINE('',#12635,#2600);
#2186=LINE('',#12637,#2601);
#2187=LINE('',#12638,#2602);
#2188=LINE('',#12641,#2603);
#2189=LINE('',#12643,#2604);
#2190=LINE('',#12644,#2605);
#2191=LINE('',#12647,#2606);
#2192=LINE('',#12649,#2607);
#2193=LINE('',#12650,#2608);
#2194=LINE('',#12652,#2609);
#2195=LINE('',#12653,#2610);
#2196=LINE('',#12665,#2611);
#2197=LINE('',#12669,#2612);
#2198=LINE('',#12673,#2613);
#2199=LINE('',#12680,#2614);
#2200=LINE('',#12682,#2615);
#2593=VECTOR('',#9832,1.);
#2594=VECTOR('',#9833,1.);
#2595=VECTOR('',#9834,1.);
#2596=VECTOR('',#9835,1.);
#2597=VECTOR('',#9838,1.);
#2598=VECTOR('',#9839,1.);
#2599=VECTOR('',#9840,1.);
#2600=VECTOR('',#9843,1.);
#2601=VECTOR('',#9844,1.);
#2602=VECTOR('',#9845,1.);
#2603=VECTOR('',#9848,1.);
#2604=VECTOR('',#9849,1.);
#2605=VECTOR('',#9850,1.);
#2606=VECTOR('',#9853,1.);
#2607=VECTOR('',#9854,1.);
#2608=VECTOR('',#9855,1.);
#2609=VECTOR('',#9858,1.);
#2610=VECTOR('',#9859,1.);
#2611=VECTOR('',#9876,0.325);
#2612=VECTOR('',#9881,0.35);
#2613=VECTOR('',#9886,0.335);
#2614=VECTOR('',#9895,0.21);
#2615=VECTOR('',#9898,0.2);
#2964=CIRCLE('',#7783,0.1954);
#2965=CIRCLE('',#7785,0.3);
#2966=CIRCLE('',#7787,0.35);
#2967=CIRCLE('',#7789,0.35);
#2968=CIRCLE('',#7791,0.32);
#2969=CIRCLE('',#7793,0.22);
#2970=CIRCLE('',#7795,0.1954);
#3514=VERTEX_POINT('',#12619);
#3515=VERTEX_POINT('',#12620);
#3516=VERTEX_POINT('',#12622);
#3517=VERTEX_POINT('',#12624);
#3518=VERTEX_POINT('',#12628);
#3519=VERTEX_POINT('',#12630);
#3520=VERTEX_POINT('',#12634);
#3521=VERTEX_POINT('',#12636);
#3522=VERTEX_POINT('',#12640);
#3523=VERTEX_POINT('',#12642);
#3524=VERTEX_POINT('',#12646);
#3525=VERTEX_POINT('',#12648);
#3526=VERTEX_POINT('',#12657);
#3527=VERTEX_POINT('',#12660);
#3528=VERTEX_POINT('',#12663);
#3529=VERTEX_POINT('',#12667);
#3530=VERTEX_POINT('',#12671);
#3531=VERTEX_POINT('',#12675);
#3532=VERTEX_POINT('',#12678);
#4321=EDGE_CURVE('',#3514,#3515,#2178,.T.);
#4322=EDGE_CURVE('',#3515,#3516,#2179,.T.);
#4323=EDGE_CURVE('',#3516,#3517,#2180,.T.);
#4324=EDGE_CURVE('',#3514,#3517,#2181,.T.);
#4325=EDGE_CURVE('',#3515,#3518,#2182,.T.);
#4326=EDGE_CURVE('',#3518,#3519,#2183,.T.);
#4327=EDGE_CURVE('',#3519,#3516,#2184,.T.);
#4328=EDGE_CURVE('',#3518,#3520,#2185,.T.);
#4329=EDGE_CURVE('',#3520,#3521,#2186,.T.);
#4330=EDGE_CURVE('',#3521,#3519,#2187,.T.);
#4331=EDGE_CURVE('',#3520,#3522,#2188,.T.);
#4332=EDGE_CURVE('',#3522,#3523,#2189,.T.);
#4333=EDGE_CURVE('',#3523,#3521,#2190,.T.);
#4334=EDGE_CURVE('',#3522,#3524,#2191,.T.);
#4335=EDGE_CURVE('',#3524,#3525,#2192,.T.);
#4336=EDGE_CURVE('',#3525,#3523,#2193,.T.);
#4337=EDGE_CURVE('',#3524,#3514,#2194,.T.);
#4338=EDGE_CURVE('',#3517,#3525,#2195,.T.);
#4339=EDGE_CURVE('',#3526,#3526,#2964,.T.);
#4340=EDGE_CURVE('',#3527,#3527,#2965,.T.);
#4341=EDGE_CURVE('',#3528,#3528,#2966,.T.);
#4342=EDGE_CURVE('',#3528,#3527,#2196,.T.);
#4343=EDGE_CURVE('',#3529,#3529,#2967,.T.);
#4344=EDGE_CURVE('',#3529,#3528,#2197,.T.);
#4345=EDGE_CURVE('',#3530,#3530,#2968,.T.);
#4346=EDGE_CURVE('',#3530,#3529,#2198,.T.);
#4347=EDGE_CURVE('',#3531,#3531,#2969,.T.);
#4348=EDGE_CURVE('',#3532,#3532,#2970,.F.);
#4349=EDGE_CURVE('',#3532,#3531,#2199,.T.);
#4350=EDGE_CURVE('',#3526,#3532,#2200,.T.);
#5927=ORIENTED_EDGE('',*,*,#4321,.T.);
#5928=ORIENTED_EDGE('',*,*,#4322,.T.);
#5929=ORIENTED_EDGE('',*,*,#4323,.T.);
#5930=ORIENTED_EDGE('',*,*,#4324,.F.);
#5931=ORIENTED_EDGE('',*,*,#4325,.T.);
#5932=ORIENTED_EDGE('',*,*,#4326,.T.);
#5933=ORIENTED_EDGE('',*,*,#4327,.T.);
#5934=ORIENTED_EDGE('',*,*,#4322,.F.);
#5935=ORIENTED_EDGE('',*,*,#4328,.T.);
#5936=ORIENTED_EDGE('',*,*,#4329,.T.);
#5937=ORIENTED_EDGE('',*,*,#4330,.T.);
#5938=ORIENTED_EDGE('',*,*,#4326,.F.);
#5939=ORIENTED_EDGE('',*,*,#4331,.T.);
#5940=ORIENTED_EDGE('',*,*,#4332,.T.);
#5941=ORIENTED_EDGE('',*,*,#4333,.T.);
#5942=ORIENTED_EDGE('',*,*,#4329,.F.);
#5943=ORIENTED_EDGE('',*,*,#4334,.T.);
#5944=ORIENTED_EDGE('',*,*,#4335,.T.);
#5945=ORIENTED_EDGE('',*,*,#4336,.T.);
#5946=ORIENTED_EDGE('',*,*,#4332,.F.);
#5947=ORIENTED_EDGE('',*,*,#4337,.T.);
#5948=ORIENTED_EDGE('',*,*,#4324,.T.);
#5949=ORIENTED_EDGE('',*,*,#4338,.T.);
#5950=ORIENTED_EDGE('',*,*,#4335,.F.);
#5951=ORIENTED_EDGE('',*,*,#4337,.F.);
#5952=ORIENTED_EDGE('',*,*,#4334,.F.);
#5953=ORIENTED_EDGE('',*,*,#4331,.F.);
#5954=ORIENTED_EDGE('',*,*,#4328,.F.);
#5955=ORIENTED_EDGE('',*,*,#4325,.F.);
#5956=ORIENTED_EDGE('',*,*,#4321,.F.);
#5957=ORIENTED_EDGE('',*,*,#4338,.F.);
#5958=ORIENTED_EDGE('',*,*,#4323,.F.);
#5959=ORIENTED_EDGE('',*,*,#4327,.F.);
#5960=ORIENTED_EDGE('',*,*,#4330,.F.);
#5961=ORIENTED_EDGE('',*,*,#4333,.F.);
#5962=ORIENTED_EDGE('',*,*,#4336,.F.);
#5963=ORIENTED_EDGE('',*,*,#4339,.F.);
#5964=ORIENTED_EDGE('',*,*,#4340,.F.);
#5965=ORIENTED_EDGE('',*,*,#4341,.F.);
#5966=ORIENTED_EDGE('',*,*,#4342,.T.);
#5967=ORIENTED_EDGE('',*,*,#4340,.T.);
#5968=ORIENTED_EDGE('',*,*,#4342,.F.);
#5969=ORIENTED_EDGE('',*,*,#4343,.F.);
#5970=ORIENTED_EDGE('',*,*,#4344,.T.);
#5971=ORIENTED_EDGE('',*,*,#4341,.T.);
#5972=ORIENTED_EDGE('',*,*,#4344,.F.);
#5973=ORIENTED_EDGE('',*,*,#4345,.F.);
#5974=ORIENTED_EDGE('',*,*,#4346,.T.);
#5975=ORIENTED_EDGE('',*,*,#4343,.T.);
#5976=ORIENTED_EDGE('',*,*,#4346,.F.);
#5977=ORIENTED_EDGE('',*,*,#4345,.T.);
#5978=ORIENTED_EDGE('',*,*,#4347,.F.);
#5979=ORIENTED_EDGE('',*,*,#4348,.F.);
#5980=ORIENTED_EDGE('',*,*,#4349,.T.);
#5981=ORIENTED_EDGE('',*,*,#4347,.T.);
#5982=ORIENTED_EDGE('',*,*,#4349,.F.);
#5983=ORIENTED_EDGE('',*,*,#4339,.T.);
#5984=ORIENTED_EDGE('',*,*,#4350,.T.);
#5985=ORIENTED_EDGE('',*,*,#4348,.T.);
#5986=ORIENTED_EDGE('',*,*,#4350,.F.);
#6098=CYLINDRICAL_SURFACE('',#7788,0.35);
#6099=CYLINDRICAL_SURFACE('',#7796,0.1954);
#6479=ADVANCED_FACE('',(#1254),#864,.F.);
#6480=ADVANCED_FACE('',(#1255),#865,.F.);
#6481=ADVANCED_FACE('',(#1256),#866,.F.);
#6482=ADVANCED_FACE('',(#1257),#867,.F.);
#6483=ADVANCED_FACE('',(#1258),#868,.F.);
#6484=ADVANCED_FACE('',(#1259),#869,.F.);
#6485=ADVANCED_FACE('',(#1260),#870,.F.);
#6486=ADVANCED_FACE('',(#1261),#871,.F.);
#6487=ADVANCED_FACE('',(#1262),#872,.F.);
#6488=ADVANCED_FACE('',(#1263),#873,.T.);
#6489=ADVANCED_FACE('',(#1264),#345,.T.);
#6490=ADVANCED_FACE('',(#1265),#6098,.T.);
#6491=ADVANCED_FACE('',(#1266),#346,.T.);
#6492=ADVANCED_FACE('',(#1267,#651),#874,.T.);
#6493=ADVANCED_FACE('',(#1268),#347,.T.);
#6494=ADVANCED_FACE('',(#1269),#6099,.T.);
#6550=CLOSED_SHELL('',(#6479,#6480,#6481,#6482,#6483,#6484,#6485,#6486));
#6551=CLOSED_SHELL('',(#6487,#6488,#6489,#6490,#6491,#6492,#6493,#6494));
#7773=AXIS2_PLACEMENT_3D('',#12617,#9828,#9829);
#7774=AXIS2_PLACEMENT_3D('',#12618,#9830,#9831);
#7775=AXIS2_PLACEMENT_3D('',#12627,#9836,#9837);
#7776=AXIS2_PLACEMENT_3D('',#12633,#9841,#9842);
#7777=AXIS2_PLACEMENT_3D('',#12639,#9846,#9847);
#7778=AXIS2_PLACEMENT_3D('',#12645,#9851,#9852);
#7779=AXIS2_PLACEMENT_3D('',#12651,#9856,#9857);
#7780=AXIS2_PLACEMENT_3D('',#12654,#9860,#9861);
#7781=AXIS2_PLACEMENT_3D('',#12655,#9862,#9863);
#7782=AXIS2_PLACEMENT_3D('',#12656,#9864,#9865);
#7783=AXIS2_PLACEMENT_3D('',#12658,#9866,#9867);
#7784=AXIS2_PLACEMENT_3D('',#12659,#9868,#9869);
#7785=AXIS2_PLACEMENT_3D('',#12661,#9870,#9871);
#7786=AXIS2_PLACEMENT_3D('',#12662,#9872,#9873);
#7787=AXIS2_PLACEMENT_3D('',#12664,#9874,#9875);
#7788=AXIS2_PLACEMENT_3D('',#12666,#9877,#9878);
#7789=AXIS2_PLACEMENT_3D('',#12668,#9879,#9880);
#7790=AXIS2_PLACEMENT_3D('',#12670,#9882,#9883);
#7791=AXIS2_PLACEMENT_3D('',#12672,#9884,#9885);
#7792=AXIS2_PLACEMENT_3D('',#12674,#9887,#9888);
#7793=AXIS2_PLACEMENT_3D('',#12676,#9889,#9890);
#7794=AXIS2_PLACEMENT_3D('',#12677,#9891,#9892);
#7795=AXIS2_PLACEMENT_3D('',#12679,#9893,#9894);
#7796=AXIS2_PLACEMENT_3D('',#12681,#9896,#9897);
#9828=DIRECTION('axis',(0.,0.,1.));
#9829=DIRECTION('refdir',(1.,0.,0.));
#9830=DIRECTION('center_axis',(0.866025403784439,0.,-0.5));
#9831=DIRECTION('ref_axis',(0.5,0.,0.866025403784439));
#9832=DIRECTION('',(-0.5,0.,-0.866025403784439));
#9833=DIRECTION('',(0.,-1.,0.));
#9834=DIRECTION('',(0.5,0.,0.866025403784439));
#9835=DIRECTION('',(0.,-1.,0.));
#9836=DIRECTION('center_axis',(1.60246890531964E-16,0.,-1.));
#9837=DIRECTION('ref_axis',(1.,0.,1.60246890531964E-16));
#9838=DIRECTION('',(-1.,0.,-1.60246890531964E-16));
#9839=DIRECTION('',(0.,-1.,0.));
#9840=DIRECTION('',(1.,0.,1.60246890531964E-16));
#9841=DIRECTION('center_axis',(-0.866025403784439,0.,-0.5));
#9842=DIRECTION('ref_axis',(0.5,0.,-0.866025403784439));
#9843=DIRECTION('',(-0.5,0.,0.866025403784439));
#9844=DIRECTION('',(0.,-1.,0.));
#9845=DIRECTION('',(0.5,0.,-0.866025403784439));
#9846=DIRECTION('center_axis',(-0.866025403784439,0.,0.5));
#9847=DIRECTION('ref_axis',(-0.5,0.,-0.866025403784439));
#9848=DIRECTION('',(0.5,0.,0.866025403784439));
#9849=DIRECTION('',(0.,-1.,0.));
#9850=DIRECTION('',(-0.5,0.,-0.866025403784439));
#9851=DIRECTION('center_axis',(-1.60246890531964E-16,0.,1.));
#9852=DIRECTION('ref_axis',(-1.,0.,-1.60246890531964E-16));
#9853=DIRECTION('',(1.,0.,1.60246890531964E-16));
#9854=DIRECTION('',(0.,-1.,0.));
#9855=DIRECTION('',(-1.,0.,-1.60246890531964E-16));
#9856=DIRECTION('center_axis',(0.866025403784439,0.,0.5));
#9857=DIRECTION('ref_axis',(-0.5,0.,0.866025403784439));
#9858=DIRECTION('',(0.5,0.,-0.866025403784439));
#9859=DIRECTION('',(-0.5,0.,0.866025403784439));
#9860=DIRECTION('center_axis',(0.,1.,0.));
#9861=DIRECTION('ref_axis',(1.,0.,0.));
#9862=DIRECTION('center_axis',(0.,-1.,0.));
#9863=DIRECTION('ref_axis',(0.,0.,-1.));
#9864=DIRECTION('center_axis',(0.,1.,0.));
#9865=DIRECTION('ref_axis',(1.,0.,0.));
#9866=DIRECTION('center_axis',(0.,1.,0.));
#9867=DIRECTION('ref_axis',(1.,0.,0.));
#9868=DIRECTION('center_axis',(0.,1.,0.));
#9869=DIRECTION('ref_axis',(0.,0.,1.));
#9870=DIRECTION('center_axis',(0.,-1.,0.));
#9871=DIRECTION('ref_axis',(1.,0.,0.));
#9872=DIRECTION('center_axis',(0.,-1.,0.));
#9873=DIRECTION('ref_axis',(1.,0.,0.));
#9874=DIRECTION('center_axis',(0.,-1.,0.));
#9875=DIRECTION('ref_axis',(1.,0.,0.));
#9876=DIRECTION('',(0.707106781186547,0.707106781186548,8.65956056235493E-17));
#9877=DIRECTION('center_axis',(0.,-1.,0.));
#9878=DIRECTION('ref_axis',(1.,0.,0.));
#9879=DIRECTION('center_axis',(0.,-1.,0.));
#9880=DIRECTION('ref_axis',(1.,0.,0.));
#9881=DIRECTION('',(0.,1.,0.));
#9882=DIRECTION('center_axis',(0.,1.,0.));
#9883=DIRECTION('ref_axis',(1.,0.,0.));
#9884=DIRECTION('center_axis',(0.,-1.,0.));
#9885=DIRECTION('ref_axis',(1.,0.,0.));
#9886=DIRECTION('',(-0.707106781186547,0.707106781186548,-8.65956056235493E-17));
#9887=DIRECTION('center_axis',(0.,-1.,0.));
#9888=DIRECTION('ref_axis',(0.,0.,-1.));
#9889=DIRECTION('center_axis',(0.,-1.,0.));
#9890=DIRECTION('ref_axis',(1.,0.,0.));
#9891=DIRECTION('center_axis',(0.,1.,0.));
#9892=DIRECTION('ref_axis',(1.,0.,0.));
#9893=DIRECTION('center_axis',(0.,1.,0.));
#9894=DIRECTION('ref_axis',(1.,0.,0.));
#9895=DIRECTION('',(-0.447213595499958,0.894427190999916,-5.47678698264203E-17));
#9896=DIRECTION('center_axis',(0.,-1.,0.));
#9897=DIRECTION('ref_axis',(1.,0.,0.));
#9898=DIRECTION('',(0.,1.,0.));
#12617=CARTESIAN_POINT('',(0.,0.,0.));
#12618=CARTESIAN_POINT('Origin',(0.0866025403784439,-0.4,-0.15));
#12619=CARTESIAN_POINT('',(0.173205080756888,-0.4,0.));
#12620=CARTESIAN_POINT('',(0.0866025403784439,-0.4,-0.15));
#12621=CARTESIAN_POINT('',(0.173205080756888,-0.4,0.));
#12622=CARTESIAN_POINT('',(0.0866025403784439,-0.64,-0.15));
#12623=CARTESIAN_POINT('',(0.0866025403784439,-0.4,-0.15));
#12624=CARTESIAN_POINT('',(0.173205080756888,-0.64,0.));
#12625=CARTESIAN_POINT('',(0.173205080756888,-0.64,0.));
#12626=CARTESIAN_POINT('',(0.173205080756888,-0.4,0.));
#12627=CARTESIAN_POINT('Origin',(-0.0866025403784438,-0.4,-0.15));
#12628=CARTESIAN_POINT('',(-0.0866025403784438,-0.4,-0.15));
#12629=CARTESIAN_POINT('',(0.0866025403784439,-0.4,-0.15));
#12630=CARTESIAN_POINT('',(-0.0866025403784438,-0.64,-0.15));
#12631=CARTESIAN_POINT('',(-0.0866025403784438,-0.4,-0.15));
#12632=CARTESIAN_POINT('',(0.0866025403784439,-0.64,-0.15));
#12633=CARTESIAN_POINT('Origin',(-0.173205080756888,-0.4,-2.77555756156289E-17));
#12634=CARTESIAN_POINT('',(-0.173205080756888,-0.4,-2.12115047744981E-17));
#12635=CARTESIAN_POINT('',(-0.0866025403784438,-0.4,-0.15));
#12636=CARTESIAN_POINT('',(-0.173205080756888,-0.64,-2.77555756156289E-17));
#12637=CARTESIAN_POINT('',(-0.173205080756888,-0.4,-2.12115047744981E-17));
#12638=CARTESIAN_POINT('',(-0.0866025403784438,-0.64,-0.15));
#12639=CARTESIAN_POINT('Origin',(-0.0866025403784439,-0.4,0.15));
#12640=CARTESIAN_POINT('',(-0.0866025403784439,-0.4,0.15));
#12641=CARTESIAN_POINT('',(-0.173205080756888,-0.4,-2.12115047744981E-17));
#12642=CARTESIAN_POINT('',(-0.0866025403784439,-0.64,0.15));
#12643=CARTESIAN_POINT('',(-0.0866025403784439,-0.4,0.15));
#12644=CARTESIAN_POINT('',(-0.173205080756888,-0.64,-2.12115047744981E-17));
#12645=CARTESIAN_POINT('Origin',(0.0866025403784439,-0.4,0.15));
#12646=CARTESIAN_POINT('',(0.0866025403784439,-0.4,0.15));
#12647=CARTESIAN_POINT('',(-0.0866025403784439,-0.4,0.15));
#12648=CARTESIAN_POINT('',(0.0866025403784439,-0.64,0.15));
#12649=CARTESIAN_POINT('',(0.0866025403784439,-0.4,0.15));
#12650=CARTESIAN_POINT('',(-0.0866025403784439,-0.64,0.15));
#12651=CARTESIAN_POINT('Origin',(0.173205080756888,-0.4,0.));
#12652=CARTESIAN_POINT('',(0.0866025403784439,-0.4,0.15));
#12653=CARTESIAN_POINT('',(0.0866025403784439,-0.64,0.15));
#12654=CARTESIAN_POINT('Origin',(0.,-0.4,-2.77555756156289E-17));
#12655=CARTESIAN_POINT('Origin',(0.,-0.64,-2.77555756156289E-17));
#12656=CARTESIAN_POINT('Origin',(0.,-1.,0.));
#12657=CARTESIAN_POINT('',(-0.1954,-1.,2.39295984553393E-17));
#12658=CARTESIAN_POINT('Origin',(0.,-1.,0.));
#12659=CARTESIAN_POINT('Origin',(0.3,0.4,0.));
#12660=CARTESIAN_POINT('',(-0.3,0.4,-3.67394039744206E-17));
#12661=CARTESIAN_POINT('Origin',(0.,0.4,0.));
#12662=CARTESIAN_POINT('Origin',(0.,0.375,0.));
#12663=CARTESIAN_POINT('',(-0.35,0.35,-4.28626379701573E-17));
#12664=CARTESIAN_POINT('Origin',(0.,0.35,0.));
#12665=CARTESIAN_POINT('',(-0.325,0.375,-3.9801020972289E-17));
#12666=CARTESIAN_POINT('Origin',(0.,0.19,0.));
#12667=CARTESIAN_POINT('',(-0.35,0.03,-4.28626379701574E-17));
#12668=CARTESIAN_POINT('Origin',(0.,0.03,0.));
#12669=CARTESIAN_POINT('',(-0.35,0.19,-4.28626379701574E-17));
#12670=CARTESIAN_POINT('Origin',(0.,0.0149999999999999,0.));
#12671=CARTESIAN_POINT('',(-0.32,-3.29597460435593E-17,-3.91886975727153E-17));
#12672=CARTESIAN_POINT('Origin',(0.,0.,0.));
#12673=CARTESIAN_POINT('',(-0.335,0.0149999999999999,-4.10256677714363E-17));
#12674=CARTESIAN_POINT('Origin',(0.22,0.,0.));
#12675=CARTESIAN_POINT('',(-0.22,-6.93889390390723E-18,-2.69422295812418E-17));
#12676=CARTESIAN_POINT('Origin',(0.,0.,0.));
#12677=CARTESIAN_POINT('Origin',(0.,-0.02,0.));
#12678=CARTESIAN_POINT('',(-0.1954,-0.0492,2.39295984553393E-17));
#12679=CARTESIAN_POINT('Origin',(0.,-0.0492,0.));
#12680=CARTESIAN_POINT('',(-0.21,-0.02,-2.57175827820944E-17));
#12681=CARTESIAN_POINT('Origin',(0.,-0.8,0.));
#12682=CARTESIAN_POINT('',(-0.1954,-0.8,-2.39295984553393E-17));
#12738=UNCERTAINTY_MEASURE_WITH_UNIT(LENGTH_MEASURE(0.001),#12784,
'DISTANCE_ACCURACY_VALUE',
'Maximum model space distance between geometric entities at asserted c
onnectivities');
#12739=UNCERTAINTY_MEASURE_WITH_UNIT(LENGTH_MEASURE(0.001),#12784,
'DISTANCE_ACCURACY_VALUE',
'Maximum model space distance between geometric entities at asserted c
onnectivities');
#12782=(
GEOMETRIC_REPRESENTATION_CONTEXT(3)
GLOBAL_UNCERTAINTY_ASSIGNED_CONTEXT((#12738))
GLOBAL_UNIT_ASSIGNED_CONTEXT((#12784,#12786,#12787))
REPRESENTATION_CONTEXT('','3D')
);
#12783=(
GEOMETRIC_REPRESENTATION_CONTEXT(3)
GLOBAL_UNCERTAINTY_ASSIGNED_CONTEXT((#12739))
GLOBAL_UNIT_ASSIGNED_CONTEXT((#12784,#12786,#12787))
REPRESENTATION_CONTEXT('','3D')
);
#12784=(
LENGTH_UNIT()
NAMED_UNIT(*)
SI_UNIT(.CENTI.,.METRE.)
);
#12786=(
NAMED_UNIT(*)
PLANE_ANGLE_UNIT()
SI_UNIT($,.RADIAN.)
);
#12787=(
NAMED_UNIT(*)
SI_UNIT($,.STERADIAN.)
SOLID_ANGLE_UNIT()
);
#12830=SHAPE_DEFINITION_REPRESENTATION(#12917,#12973);
#12917=PRODUCT_DEFINITION_SHAPE('',$,#13017);
#12973=SHAPE_REPRESENTATION('',(#7773),#12782);
#12974=PRODUCT_DEFINITION_CONTEXT('part definition',#13105,'design');
#13017=PRODUCT_DEFINITION('M4x10 Cap Screw','M4x10 Cap Screw',#13060,#12974);
#13060=PRODUCT_DEFINITION_FORMATION('',$,#13149);
#13105=APPLICATION_CONTEXT(
'Core Data for Automotive Mechanical Design Process');
#13106=PRODUCT_CONTEXT('part definition',#13105,'mechanical');
#13149=PRODUCT('M4x10 Cap Screw','M4x10 Cap Screw','M4x10 Cap Screw',(#13106));
#13213=COLOUR_RGB('Black',0.12,0.14,0.17);
#13214=FILL_AREA_STYLE_COLOUR('',#13213);
#13215=FILL_AREA_STYLE('',(#13214));
#13216=SURFACE_STYLE_FILL_AREA(#13215);
#13217=SURFACE_SIDE_STYLE('',(#13216));
#13218=SURFACE_STYLE_USAGE(.BOTH.,#13217);
#13219=PRESENTATION_STYLE_ASSIGNMENT((#13218));
ENDSEC;
END-ISO-10303-21;
